ISO-10303-21;
HEADER;
/* Generated by software containing ST-Developer
 * from STEP Tools, Inc. (www.steptools.com) 
 */

FILE_DESCRIPTION(
/* description */ ('Counter shaft with two pulleys and keyed hub'),
/* implementation_level */ '2;1');

FILE_NAME(
/* name */ 'Socket Set Screw - M5x8.step',
/* time_stamp */ '2026-10-27T10:46:10-07:00',
/* author */ (''),
/* organization */ (''),
/* preprocessor_version */ 'ST-DEVELOPER v20.2',
/* originating_system */ 'Autodesk Translation Framework v15.17.0.0',
/* authorisation */ '');

FILE_SCHEMA (('AUTOMOTIVE_DESIGN { 1 0 10303 214 3 1 1 }'));
ENDSEC;

DATA;
#10=MECHANICAL_DESIGN_GEOMETRIC_PRESENTATION_REPRESENTATION('',(#315),#10821);
#18=CONICAL_SURFACE('',#6531,0.235,0.785398163397448);
#19=CONICAL_SURFACE('',#6535,0.2125,0.785398163397448);
#264=SHAPE_REPRESENTATION_RELATIONSHIP('SRR','None',#10952,#289);
#289=ADVANCED_BREP_SHAPE_REPRESENTATION('',(#339),#10820);
#315=STYLED_ITEM('',(#11142),#339);
#339=MANIFOLD_SOLID_BREP('Body1',#5600);
#430=FACE_BOUND('',#1302,.T.);
#579=PLANE('',#6522);
#580=PLANE('',#6523);
#581=PLANE('',#6524);
#582=PLANE('',#6525);
#583=PLANE('',#6526);
#584=PLANE('',#6527);
#585=PLANE('',#6528);
#586=PLANE('',#6529);
#587=PLANE('',#6537);
#890=FACE_OUTER_BOUND('',#1294,.T.);
#891=FACE_OUTER_BOUND('',#1295,.T.);
#892=FACE_OUTER_BOUND('',#1296,.T.);
#893=FACE_OUTER_BOUND('',#1297,.T.);
#894=FACE_OUTER_BOUND('',#1298,.T.);
#895=FACE_OUTER_BOUND('',#1299,.T.);
#896=FACE_OUTER_BOUND('',#1300,.T.);
#897=FACE_OUTER_BOUND('',#1301,.T.);
#898=FACE_OUTER_BOUND('',#1303,.T.);
#899=FACE_OUTER_BOUND('',#1304,.T.);
#900=FACE_OUTER_BOUND('',#1305,.T.);
#901=FACE_OUTER_BOUND('',#1306,.T.);
#1294=EDGE_LOOP('',(#5063,#5064,#5065,#5066));
#1295=EDGE_LOOP('',(#5067,#5068,#5069,#5070));
#1296=EDGE_LOOP('',(#5071,#5072,#5073,#5074));
#1297=EDGE_LOOP('',(#5075,#5076,#5077,#5078));
#1298=EDGE_LOOP('',(#5079,#5080,#5081,#5082));
#1299=EDGE_LOOP('',(#5083,#5084,#5085,#5086));
#1300=EDGE_LOOP('',(#5087,#5088,#5089,#5090,#5091,#5092));
#1301=EDGE_LOOP('',(#5093));
#1302=EDGE_LOOP('',(#5094,#5095,#5096,#5097,#5098,#5099));
#1303=EDGE_LOOP('',(#5100,#5101,#5102,#5103));
#1304=EDGE_LOOP('',(#5104,#5105,#5106,#5107));
#1305=EDGE_LOOP('',(#5108,#5109,#5110,#5111));
#1306=EDGE_LOOP('',(#5112));
#1675=LINE('',#10691,#2064);
#1676=LINE('',#10693,#2065);
#1677=LINE('',#10695,#2066);
#1678=LINE('',#10696,#2067);
#1679=LINE('',#10699,#2068);
#1680=LINE('',#10701,#2069);
#1681=LINE('',#10702,#2070);
#1682=LINE('',#10705,#2071);
#1683=LINE('',#10707,#2072);
#1684=LINE('',#10708,#2073);
#1685=LINE('',#10711,#2074);
#1686=LINE('',#10713,#2075);
#1687=LINE('',#10714,#2076);
#1688=LINE('',#10717,#2077);
#1689=LINE('',#10719,#2078);
#1690=LINE('',#10720,#2079);
#1691=LINE('',#10722,#2080);
#1692=LINE('',#10723,#2081);
#1693=LINE('',#10731,#2082);
#1694=LINE('',#10735,#2083);
#1695=LINE('',#10739,#2084);
#2064=VECTOR('',#8219,1.);
#2065=VECTOR('',#8220,1.);
#2066=VECTOR('',#8221,1.);
#2067=VECTOR('',#8222,1.);
#2068=VECTOR('',#8225,1.);
#2069=VECTOR('',#8226,1.);
#2070=VECTOR('',#8227,1.);
#2071=VECTOR('',#8230,1.);
#2072=VECTOR('',#8231,1.);
#2073=VECTOR('',#8232,1.);
#2074=VECTOR('',#8235,1.);
#2075=VECTOR('',#8236,1.);
#2076=VECTOR('',#8237,1.);
#2077=VECTOR('',#8240,1.);
#2078=VECTOR('',#8241,1.);
#2079=VECTOR('',#8242,1.);
#2080=VECTOR('',#8245,1.);
#2081=VECTOR('',#8246,1.);
#2082=VECTOR('',#8257,0.235);
#2083=VECTOR('',#8262,0.25);
#2084=VECTOR('',#8267,0.2125);
#2380=CIRCLE('',#6530,0.22);
#2381=CIRCLE('',#6532,0.24505);
#2382=CIRCLE('',#6534,0.24505);
#2383=CIRCLE('',#6536,0.175);
#2871=VERTEX_POINT('',#10689);
#2872=VERTEX_POINT('',#10690);
#2873=VERTEX_POINT('',#10692);
#2874=VERTEX_POINT('',#10694);
#2875=VERTEX_POINT('',#10698);
#2876=VERTEX_POINT('',#10700);
#2877=VERTEX_POINT('',#10704);
#2878=VERTEX_POINT('',#10706);
#2879=VERTEX_POINT('',#10710);
#2880=VERTEX_POINT('',#10712);
#2881=VERTEX_POINT('',#10716);
#2882=VERTEX_POINT('',#10718);
#2883=VERTEX_POINT('',#10726);
#2884=VERTEX_POINT('',#10729);
#2885=VERTEX_POINT('',#10733);
#2886=VERTEX_POINT('',#10737);
#3604=EDGE_CURVE('',#2871,#2872,#1675,.T.);
#3605=EDGE_CURVE('',#2871,#2873,#1676,.T.);
#3606=EDGE_CURVE('',#2873,#2874,#1677,.T.);
#3607=EDGE_CURVE('',#2872,#2874,#1678,.T.);
#3608=EDGE_CURVE('',#2875,#2871,#1679,.T.);
#3609=EDGE_CURVE('',#2875,#2876,#1680,.T.);
#3610=EDGE_CURVE('',#2876,#2873,#1681,.T.);
#3611=EDGE_CURVE('',#2877,#2875,#1682,.T.);
#3612=EDGE_CURVE('',#2877,#2878,#1683,.T.);
#3613=EDGE_CURVE('',#2878,#2876,#1684,.T.);
#3614=EDGE_CURVE('',#2879,#2877,#1685,.T.);
#3615=EDGE_CURVE('',#2879,#2880,#1686,.T.);
#3616=EDGE_CURVE('',#2880,#2878,#1687,.T.);
#3617=EDGE_CURVE('',#2881,#2879,#1688,.T.);
#3618=EDGE_CURVE('',#2881,#2882,#1689,.T.);
#3619=EDGE_CURVE('',#2882,#2880,#1690,.T.);
#3620=EDGE_CURVE('',#2872,#2881,#1691,.T.);
#3621=EDGE_CURVE('',#2874,#2882,#1692,.T.);
#3622=EDGE_CURVE('',#2883,#2883,#2380,.T.);
#3623=EDGE_CURVE('',#2884,#2884,#2381,.T.);
#3624=EDGE_CURVE('',#2884,#2883,#1693,.T.);
#3625=EDGE_CURVE('',#2885,#2885,#2382,.F.);
#3626=EDGE_CURVE('',#2885,#2884,#1694,.T.);
#3627=EDGE_CURVE('',#2886,#2886,#2383,.T.);
#3628=EDGE_CURVE('',#2886,#2885,#1695,.T.);
#5063=ORIENTED_EDGE('',*,*,#3604,.F.);
#5064=ORIENTED_EDGE('',*,*,#3605,.T.);
#5065=ORIENTED_EDGE('',*,*,#3606,.T.);
#5066=ORIENTED_EDGE('',*,*,#3607,.F.);
#5067=ORIENTED_EDGE('',*,*,#3608,.F.);
#5068=ORIENTED_EDGE('',*,*,#3609,.T.);
#5069=ORIENTED_EDGE('',*,*,#3610,.T.);
#5070=ORIENTED_EDGE('',*,*,#3605,.F.);
#5071=ORIENTED_EDGE('',*,*,#3611,.F.);
#5072=ORIENTED_EDGE('',*,*,#3612,.T.);
#5073=ORIENTED_EDGE('',*,*,#3613,.T.);
#5074=ORIENTED_EDGE('',*,*,#3609,.F.);
#5075=ORIENTED_EDGE('',*,*,#3614,.F.);
#5076=ORIENTED_EDGE('',*,*,#3615,.T.);
#5077=ORIENTED_EDGE('',*,*,#3616,.T.);
#5078=ORIENTED_EDGE('',*,*,#3612,.F.);
#5079=ORIENTED_EDGE('',*,*,#3617,.F.);
#5080=ORIENTED_EDGE('',*,*,#3618,.T.);
#5081=ORIENTED_EDGE('',*,*,#3619,.T.);
#5082=ORIENTED_EDGE('',*,*,#3615,.F.);
#5083=ORIENTED_EDGE('',*,*,#3620,.F.);
#5084=ORIENTED_EDGE('',*,*,#3607,.T.);
#5085=ORIENTED_EDGE('',*,*,#3621,.T.);
#5086=ORIENTED_EDGE('',*,*,#3618,.F.);
#5087=ORIENTED_EDGE('',*,*,#3621,.F.);
#5088=ORIENTED_EDGE('',*,*,#3606,.F.);
#5089=ORIENTED_EDGE('',*,*,#3610,.F.);
#5090=ORIENTED_EDGE('',*,*,#3613,.F.);
#5091=ORIENTED_EDGE('',*,*,#3616,.F.);
#5092=ORIENTED_EDGE('',*,*,#3619,.F.);
#5093=ORIENTED_EDGE('',*,*,#3622,.F.);
#5094=ORIENTED_EDGE('',*,*,#3604,.T.);
#5095=ORIENTED_EDGE('',*,*,#3620,.T.);
#5096=ORIENTED_EDGE('',*,*,#3617,.T.);
#5097=ORIENTED_EDGE('',*,*,#3614,.T.);
#5098=ORIENTED_EDGE('',*,*,#3611,.T.);
#5099=ORIENTED_EDGE('',*,*,#3608,.T.);
#5100=ORIENTED_EDGE('',*,*,#3623,.F.);
#5101=ORIENTED_EDGE('',*,*,#3624,.T.);
#5102=ORIENTED_EDGE('',*,*,#3622,.T.);
#5103=ORIENTED_EDGE('',*,*,#3624,.F.);
#5104=ORIENTED_EDGE('',*,*,#3625,.F.);
#5105=ORIENTED_EDGE('',*,*,#3626,.T.);
#5106=ORIENTED_EDGE('',*,*,#3623,.T.);
#5107=ORIENTED_EDGE('',*,*,#3626,.F.);
#5108=ORIENTED_EDGE('',*,*,#3627,.F.);
#5109=ORIENTED_EDGE('',*,*,#3628,.T.);
#5110=ORIENTED_EDGE('',*,*,#3625,.T.);
#5111=ORIENTED_EDGE('',*,*,#3628,.F.);
#5112=ORIENTED_EDGE('',*,*,#3627,.T.);
#5258=CYLINDRICAL_SURFACE('',#6533,0.24505);
#5561=ADVANCED_FACE('',(#890),#579,.F.);
#5562=ADVANCED_FACE('',(#891),#580,.F.);
#5563=ADVANCED_FACE('',(#892),#581,.F.);
#5564=ADVANCED_FACE('',(#893),#582,.F.);
#5565=ADVANCED_FACE('',(#894),#583,.F.);
#5566=ADVANCED_FACE('',(#895),#584,.F.);
#5567=ADVANCED_FACE('',(#896),#585,.F.);
#5568=ADVANCED_FACE('',(#897,#430),#586,.T.);
#5569=ADVANCED_FACE('',(#898),#18,.T.);
#5570=ADVANCED_FACE('',(#899),#5258,.T.);
#5571=ADVANCED_FACE('',(#900),#19,.T.);
#5572=ADVANCED_FACE('',(#901),#587,.T.);
#5600=CLOSED_SHELL('',(#5561,#5562,#5563,#5564,#5565,#5566,#5567,#5568,
#5569,#5570,#5571,#5572));
#6521=AXIS2_PLACEMENT_3D('',#10687,#8215,#8216);
#6522=AXIS2_PLACEMENT_3D('',#10688,#8217,#8218);
#6523=AXIS2_PLACEMENT_3D('',#10697,#8223,#8224);
#6524=AXIS2_PLACEMENT_3D('',#10703,#8228,#8229);
#6525=AXIS2_PLACEMENT_3D('',#10709,#8233,#8234);
#6526=AXIS2_PLACEMENT_3D('',#10715,#8238,#8239);
#6527=AXIS2_PLACEMENT_3D('',#10721,#8243,#8244);
#6528=AXIS2_PLACEMENT_3D('',#10724,#8247,#8248);
#6529=AXIS2_PLACEMENT_3D('',#10725,#8249,#8250);
#6530=AXIS2_PLACEMENT_3D('',#10727,#8251,#8252);
#6531=AXIS2_PLACEMENT_3D('',#10728,#8253,#8254);
#6532=AXIS2_PLACEMENT_3D('',#10730,#8255,#8256);
#6533=AXIS2_PLACEMENT_3D('',#10732,#8258,#8259);
#6534=AXIS2_PLACEMENT_3D('',#10734,#8260,#8261);
#6535=AXIS2_PLACEMENT_3D('',#10736,#8263,#8264);
#6536=AXIS2_PLACEMENT_3D('',#10738,#8265,#8266);
#6537=AXIS2_PLACEMENT_3D('',#10740,#8268,#8269);
#8215=DIRECTION('axis',(0.,0.,1.));
#8216=DIRECTION('refdir',(1.,0.,0.));
#8217=DIRECTION('center_axis',(0.866025403784439,0.,-0.5));
#8218=DIRECTION('ref_axis',(0.5,0.,0.866025403784439));
#8219=DIRECTION('',(0.5,0.,0.866025403784439));
#8220=DIRECTION('',(0.,-1.,0.));
#8221=DIRECTION('',(0.5,0.,0.866025403784439));
#8222=DIRECTION('',(0.,-1.,0.));
#8223=DIRECTION('center_axis',(1.92296268638356E-16,0.,-1.));
#8224=DIRECTION('ref_axis',(1.,0.,1.92296268638356E-16));
#8225=DIRECTION('',(1.,0.,1.92296268638356E-16));
#8226=DIRECTION('',(0.,-1.,0.));
#8227=DIRECTION('',(1.,0.,1.92296268638356E-16));
#8228=DIRECTION('center_axis',(-0.866025403784439,0.,-0.5));
#8229=DIRECTION('ref_axis',(0.5,0.,-0.866025403784439));
#8230=DIRECTION('',(0.5,0.,-0.866025403784439));
#8231=DIRECTION('',(0.,-1.,0.));
#8232=DIRECTION('',(0.5,0.,-0.866025403784438));
#8233=DIRECTION('center_axis',(-0.866025403784439,0.,0.5));
#8234=DIRECTION('ref_axis',(-0.5,0.,-0.866025403784439));
#8235=DIRECTION('',(-0.5,0.,-0.866025403784439));
#8236=DIRECTION('',(0.,-1.,0.));
#8237=DIRECTION('',(-0.5,0.,-0.866025403784439));
#8238=DIRECTION('center_axis',(-1.92296268638356E-16,0.,1.));
#8239=DIRECTION('ref_axis',(-1.,0.,-1.92296268638356E-16));
#8240=DIRECTION('',(-1.,0.,-1.92296268638356E-16));
#8241=DIRECTION('',(0.,-1.,0.));
#8242=DIRECTION('',(-1.,0.,-1.92296268638356E-16));
#8243=DIRECTION('center_axis',(0.866025403784439,0.,0.5));
#8244=DIRECTION('ref_axis',(-0.5,0.,0.866025403784439));
#8245=DIRECTION('',(-0.5,0.,0.866025403784439));
#8246=DIRECTION('',(-0.5,0.,0.866025403784439));
#8247=DIRECTION('center_axis',(0.,-1.,0.));
#8248=DIRECTION('ref_axis',(0.,0.,-1.));
#8249=DIRECTION('center_axis',(0.,1.,0.));
#8250=DIRECTION('ref_axis',(0.,0.,1.));
#8251=DIRECTION('center_axis',(0.,-1.,0.));
#8252=DIRECTION('ref_axis',(1.,0.,0.));
#8253=DIRECTION('center_axis',(0.,-1.,0.));
#8254=DIRECTION('ref_axis',(1.,0.,0.));
#8255=DIRECTION('center_axis',(0.,-1.,0.));
#8256=DIRECTION('ref_axis',(1.,0.,0.));
#8257=DIRECTION('',(0.707106781186547,0.707106781186548,8.65956056235493E-17));
#8258=DIRECTION('center_axis',(0.,-1.,0.));
#8259=DIRECTION('ref_axis',(1.,0.,0.));
#8260=DIRECTION('center_axis',(0.,1.,0.));
#8261=DIRECTION('ref_axis',(1.,0.,0.));
#8262=DIRECTION('',(0.,1.,0.));
#8263=DIRECTION('center_axis',(0.,1.,0.));
#8264=DIRECTION('ref_axis',(1.,0.,0.));
#8265=DIRECTION('center_axis',(0.,-1.,0.));
#8266=DIRECTION('ref_axis',(1.,0.,0.));
#8267=DIRECTION('',(-0.707106781186547,0.707106781186548,-8.65956056235493E-17));
#8268=DIRECTION('center_axis',(0.,-1.,0.));
#8269=DIRECTION('ref_axis',(0.,0.,-1.));
#10687=CARTESIAN_POINT('',(0.,0.,0.));
#10688=CARTESIAN_POINT('Origin',(0.0721687836487032,0.,-0.125));
#10689=CARTESIAN_POINT('',(0.0721687836487032,0.,-0.125));
#10690=CARTESIAN_POINT('',(0.144337567297406,0.,0.));
#10691=CARTESIAN_POINT('',(0.117710979560879,0.,-0.0461186027918559));
#10692=CARTESIAN_POINT('',(0.0721687836487032,-0.25,-0.125));
#10693=CARTESIAN_POINT('',(0.0721687836487032,0.,-0.125));
#10694=CARTESIAN_POINT('',(0.144337567297406,-0.25,0.));
#10695=CARTESIAN_POINT('',(0.144337567297406,-0.25,0.));
#10696=CARTESIAN_POINT('',(0.144337567297406,0.,0.));
#10697=CARTESIAN_POINT('Origin',(-0.0721687836487032,0.,-0.125));
#10698=CARTESIAN_POINT('',(-0.0721687836487032,0.,-0.125));
#10699=CARTESIAN_POINT('',(0.0739156081756484,0.,-0.125));
#10700=CARTESIAN_POINT('',(-0.0721687836487032,-0.25,-0.125));
#10701=CARTESIAN_POINT('',(-0.0721687836487032,0.,-0.125));
#10702=CARTESIAN_POINT('',(0.0721687836487032,-0.25,-0.125));
#10703=CARTESIAN_POINT('Origin',(-0.144337567297406,0.,-4.16333634234434E-17));
#10704=CARTESIAN_POINT('',(-0.144337567297406,0.,-1.76762539787485E-17));
#10705=CARTESIAN_POINT('',(-0.0987953713852306,0.,-0.0788813972081442));
#10706=CARTESIAN_POINT('',(-0.144337567297406,-0.25,-2.77555756156289E-17));
#10707=CARTESIAN_POINT('',(-0.144337567297406,0.,-1.76762539787485E-17));
#10708=CARTESIAN_POINT('',(-0.0721687836487032,-0.25,-0.125));
#10709=CARTESIAN_POINT('Origin',(-0.0721687836487033,0.,0.125));
#10710=CARTESIAN_POINT('',(-0.0721687836487033,0.,0.125));
#10711=CARTESIAN_POINT('',(-0.0627109795608791,0.,0.141381397208144));
#10712=CARTESIAN_POINT('',(-0.0721687836487033,-0.25,0.125));
#10713=CARTESIAN_POINT('',(-0.0721687836487033,0.,0.125));
#10714=CARTESIAN_POINT('',(-0.144337567297406,-0.25,-1.76762539787485E-17));
#10715=CARTESIAN_POINT('Origin',(0.0721687836487032,0.,0.125));
#10716=CARTESIAN_POINT('',(0.0721687836487032,0.,0.125));
#10717=CARTESIAN_POINT('',(0.146084391824352,0.,0.125));
#10718=CARTESIAN_POINT('',(0.0721687836487032,-0.25,0.125));
#10719=CARTESIAN_POINT('',(0.0721687836487032,0.,0.125));
#10720=CARTESIAN_POINT('',(-0.0721687836487033,-0.25,0.125));
#10721=CARTESIAN_POINT('Origin',(0.144337567297406,0.,0.));
#10722=CARTESIAN_POINT('',(0.153795371385231,0.,-0.0163813972081441));
#10723=CARTESIAN_POINT('',(0.0721687836487032,-0.25,0.125));
#10724=CARTESIAN_POINT('Origin',(0.,-0.25,0.));
#10725=CARTESIAN_POINT('Origin',(0.22,0.,0.));
#10726=CARTESIAN_POINT('',(-0.22,-8.67361737988404E-18,-2.69422295812418E-17));
#10727=CARTESIAN_POINT('Origin',(0.,0.,0.));
#10728=CARTESIAN_POINT('Origin',(0.,-0.015,0.));
#10729=CARTESIAN_POINT('',(-0.24505,-0.02505,-3.00099698131059E-17));
#10730=CARTESIAN_POINT('Origin',(0.,-0.02505,0.));
#10731=CARTESIAN_POINT('',(-0.235,-0.015,-2.87791997799628E-17));
#10732=CARTESIAN_POINT('Origin',(0.,-0.3775,0.));
#10733=CARTESIAN_POINT('',(-0.24505,-0.72995,3.00099698131059E-17));
#10734=CARTESIAN_POINT('Origin',(0.,-0.72995,0.));
#10735=CARTESIAN_POINT('',(-0.24505,-0.3775,-3.00099698131059E-17));
#10736=CARTESIAN_POINT('Origin',(0.,-0.7625,0.));
#10737=CARTESIAN_POINT('',(-0.175,-0.8,-2.14313189850787E-17));
#10738=CARTESIAN_POINT('Origin',(0.,-0.8,0.));
#10739=CARTESIAN_POINT('',(-0.2125,-0.7625,-2.60237444818813E-17));
#10740=CARTESIAN_POINT('Origin',(0.,-0.8,0.));
#10790=UNCERTAINTY_MEASURE_WITH_UNIT(LENGTH_MEASURE(0.001),#10822,
'DISTANCE_ACCURACY_VALUE',
'Maximum model space distance between geometric entities at asserted c
onnectivities');
#10791=UNCERTAINTY_MEASURE_WITH_UNIT(LENGTH_MEASURE(0.001),#10822,
'DISTANCE_ACCURACY_VALUE',
'Maximum model space distance between geometric entities at asserted c
onnectivities');
#10820=(
GEOMETRIC_REPRESENTATION_CONTEXT(3)
GLOBAL_UNCERTAINTY_ASSIGNED_CONTEXT((#10790))
GLOBAL_UNIT_ASSIGNED_CONTEXT((#10822,#10824,#10825))
REPRESENTATION_CONTEXT('','3D')
);
#10821=(
GEOMETRIC_REPRESENTATION_CONTEXT(3)
GLOBAL_UNCERTAINTY_ASSIGNED_CONTEXT((#10791))
GLOBAL_UNIT_ASSIGNED_CONTEXT((#10822,#10824,#10825))
REPRESENTATION_CONTEXT('','3D')
);
#10822=(
LENGTH_UNIT()
NAMED_UNIT(*)
SI_UNIT(.CENTI.,.METRE.)
);
#10824=(
NAMED_UNIT(*)
PLANE_ANGLE_UNIT()
SI_UNIT($,.RADIAN.)
);
#10825=(
NAMED_UNIT(*)
SI_UNIT($,.STERADIAN.)
SOLID_ANGLE_UNIT()
);
#10854=SHAPE_DEFINITION_REPRESENTATION(#10902,#10952);
#10902=PRODUCT_DEFINITION_SHAPE('',$,#10982);
#10952=SHAPE_REPRESENTATION('',(#6521),#10820);
#10953=PRODUCT_DEFINITION_CONTEXT('part definition',#11042,'design');
#10982=PRODUCT_DEFINITION('Socket Set Screw - M5x8',
'Socket Set Screw - M5x8',#11011,#10953);
#11011=PRODUCT_DEFINITION_FORMATION('',$,#11072);
#11042=APPLICATION_CONTEXT(
'Core Data for Automotive Mechanical Design Process');
#11043=PRODUCT_CONTEXT('part definition',#11042,'mechanical');
#11072=PRODUCT('Socket Set Screw - M5x8','Socket Set Screw - M5x8',
'Socket Set Screw - M5x8',(#11043));
#11136=COLOUR_RGB('Black',0.12,0.14,0.17);
#11137=FILL_AREA_STYLE_COLOUR('',#11136);
#11138=FILL_AREA_STYLE('',(#11137));
#11139=SURFACE_STYLE_FILL_AREA(#11138);
#11140=SURFACE_SIDE_STYLE('',(#11139));
#11141=SURFACE_STYLE_USAGE(.BOTH.,#11140);
#11142=PRESENTATION_STYLE_ASSIGNMENT((#11141));
ENDSEC;
END-ISO-10303-21;
